ISO-10303-21;
HEADER;
/* Generated by software containing ST-Developer
 * from STEP Tools, Inc. (www.steptools.com) 
 */

FILE_DESCRIPTION(
/* description */ ('STEP AP214'),
/* implementation_level */ '2;1');

FILE_NAME(
/* name */ 'PRT-RH-1004-03.step',
/* time_stamp */ '2026-10-07T12:49:37-07:00',
/* author */ (''),
/* organization */ (''),
/* preprocessor_version */ 'ST-DEVELOPER v20.2',
/* originating_system */ 'Autodesk Translation Framework v15.15.0.0',
/* authorisation */ '');

FILE_SCHEMA (('AUTOMOTIVE_DESIGN { 1 0 10303 214 3 1 1 }'));
ENDSEC;

DATA;
#10=MECHANICAL_DESIGN_GEOMETRIC_PRESENTATION_REPRESENTATION('',(#289),#33016);
#235=SHAPE_REPRESENTATION_RELATIONSHIP('SRR','None',#33128,#262);
#262=ADVANCED_BREP_SHAPE_REPRESENTATION('',(#320),#32989);
#289=STYLED_ITEM('',(#33284),#320);
#320=MANIFOLD_SOLID_BREP('Body1',#9944);
#349=CONICAL_SURFACE('',#10613,3.50000000000001,0.785398163397444);
#350=CONICAL_SURFACE('',#10614,3.,0.78539816339745);
#491=FACE_BOUND('',#1786,.T.);
#492=FACE_BOUND('',#1788,.T.);
#865=PLANE('',#10587);
#866=PLANE('',#10588);
#867=PLANE('',#10589);
#868=PLANE('',#10591);
#869=PLANE('',#10597);
#870=PLANE('',#10598);
#871=PLANE('',#10599);
#872=PLANE('',#10600);
#873=PLANE('',#10601);
#874=PLANE('',#10602);
#875=PLANE('',#10603);
#876=PLANE('',#10604);
#877=PLANE('',#10605);
#878=PLANE('',#10606);
#879=PLANE('',#10607);
#880=PLANE('',#10608);
#881=PLANE('',#10609);
#882=PLANE('',#10610);
#883=PLANE('',#10611);
#884=PLANE('',#10612);
#1208=FACE_OUTER_BOUND('',#1781,.T.);
#1209=FACE_OUTER_BOUND('',#1782,.T.);
#1210=FACE_OUTER_BOUND('',#1783,.T.);
#1211=FACE_OUTER_BOUND('',#1784,.T.);
#1212=FACE_OUTER_BOUND('',#1785,.T.);
#1213=FACE_OUTER_BOUND('',#1787,.T.);
#1214=FACE_OUTER_BOUND('',#1789,.T.);
#1215=FACE_OUTER_BOUND('',#1790,.T.);
#1216=FACE_OUTER_BOUND('',#1791,.T.);
#1217=FACE_OUTER_BOUND('',#1792,.T.);
#1218=FACE_OUTER_BOUND('',#1793,.T.);
#1219=FACE_OUTER_BOUND('',#1794,.T.);
#1220=FACE_OUTER_BOUND('',#1795,.T.);
#1221=FACE_OUTER_BOUND('',#1796,.T.);
#1222=FACE_OUTER_BOUND('',#1797,.T.);
#1223=FACE_OUTER_BOUND('',#1798,.T.);
#1224=FACE_OUTER_BOUND('',#1799,.T.);
#1225=FACE_OUTER_BOUND('',#1800,.T.);
#1226=FACE_OUTER_BOUND('',#1801,.T.);
#1227=FACE_OUTER_BOUND('',#1802,.T.);
#1228=FACE_OUTER_BOUND('',#1803,.T.);
#1229=FACE_OUTER_BOUND('',#1804,.T.);
#1230=FACE_OUTER_BOUND('',#1805,.T.);
#1231=FACE_OUTER_BOUND('',#1806,.T.);
#1232=FACE_OUTER_BOUND('',#1807,.T.);
#1781=EDGE_LOOP('',(#7434,#7435,#7436,#7437));
#1782=EDGE_LOOP('',(#7438,#7439,#7440,#7441));
#1783=EDGE_LOOP('',(#7442,#7443,#7444,#7445));
#1784=EDGE_LOOP('',(#7446,#7447,#7448,#7449));
#1785=EDGE_LOOP('',(#7450,#7451,#7452,#7453,#7454,#7455,#7456,#7457,#7458,
#7459,#7460,#7461,#7462,#7463,#7464,#7465,#7466,#7467,#7468,#7469));
#1786=EDGE_LOOP('',(#7470));
#1787=EDGE_LOOP('',(#7471,#7472,#7473,#7474,#7475,#7476,#7477,#7478,#7479,
#7480,#7481,#7482,#7483,#7484,#7485,#7486,#7487,#7488,#7489,#7490));
#1788=EDGE_LOOP('',(#7491));
#1789=EDGE_LOOP('',(#7492,#7493,#7494,#7495,#7496));
#1790=EDGE_LOOP('',(#7497,#7498,#7499,#7500));
#1791=EDGE_LOOP('',(#7501,#7502,#7503,#7504));
#1792=EDGE_LOOP('',(#7505,#7506,#7507,#7508));
#1793=EDGE_LOOP('',(#7509,#7510,#7511,#7512));
#1794=EDGE_LOOP('',(#7513,#7514,#7515,#7516));
#1795=EDGE_LOOP('',(#7517,#7518,#7519,#7520));
#1796=EDGE_LOOP('',(#7521,#7522,#7523,#7524));
#1797=EDGE_LOOP('',(#7525,#7526,#7527,#7528));
#1798=EDGE_LOOP('',(#7529,#7530,#7531,#7532));
#1799=EDGE_LOOP('',(#7533,#7534,#7535,#7536));
#1800=EDGE_LOOP('',(#7537,#7538,#7539,#7540));
#1801=EDGE_LOOP('',(#7541,#7542,#7543,#7544));
#1802=EDGE_LOOP('',(#7545,#7546,#7547,#7548));
#1803=EDGE_LOOP('',(#7549,#7550,#7551,#7552));
#1804=EDGE_LOOP('',(#7553,#7554,#7555,#7556));
#1805=EDGE_LOOP('',(#7557,#7558,#7559,#7560));
#1806=EDGE_LOOP('',(#7561,#7562,#7563,#7564,#7565));
#1807=EDGE_LOOP('',(#7566,#7567,#7568,#7569));
#2344=CIRCLE('',#10582,17.1);
#2345=CIRCLE('',#10583,17.1);
#2346=CIRCLE('',#10585,9.);
#2347=CIRCLE('',#10586,9.);
#2348=CIRCLE('',#10590,3.50000000000001);
#2349=CIRCLE('',#10592,3.50000000000001);
#2350=CIRCLE('',#10594,3.);
#2351=CIRCLE('',#10595,3.);
#2352=CIRCLE('',#10596,3.);
#2935=LINE('',#17838,#3685);
#2936=LINE('',#17842,#3686);
#2937=LINE('',#17849,#3687);
#2938=LINE('',#17852,#3688);
#2939=LINE('',#17855,#3689);
#2940=LINE('',#17857,#3690);
#2941=LINE('',#17858,#3691);
#2942=LINE('',#17861,#3692);
#2943=LINE('',#17863,#3693);
#2944=LINE('',#17864,#3694);
#2945=LINE('',#17867,#3695);
#2946=LINE('',#17869,#3696);
#2947=LINE('',#17871,#3697);
#2948=LINE('',#17873,#3698);
#2949=LINE('',#17875,#3699);
#2950=LINE('',#17877,#3700);
#2951=LINE('',#17879,#3701);
#2952=LINE('',#17880,#3702);
#2953=LINE('',#17882,#3703);
#2954=LINE('',#17884,#3704);
#2955=LINE('',#17886,#3705);
#2956=LINE('',#17888,#3706);
#2957=LINE('',#17890,#3707);
#2958=LINE('',#17892,#3708);
#2959=LINE('',#17894,#3709);
#2960=LINE('',#17895,#3710);
#2961=LINE('',#17900,#3711);
#2962=LINE('',#17902,#3712);
#2963=LINE('',#17904,#3713);
#2964=LINE('',#17906,#3714);
#2965=LINE('',#17908,#3715);
#2966=LINE('',#17910,#3716);
#2967=LINE('',#17912,#3717);
#2968=LINE('',#17913,#3718);
#2969=LINE('',#17915,#3719);
#2970=LINE('',#17917,#3720);
#2971=LINE('',#17919,#3721);
#2972=LINE('',#17921,#3722);
#2973=LINE('',#17923,#3723);
#2974=LINE('',#17925,#3724);
#2975=LINE('',#17927,#3725);
#2976=LINE('',#17928,#3726);
#2977=LINE('',#17936,#3727);
#2978=LINE('',#17940,#3728);
#2979=LINE('',#17942,#3729);
#2980=LINE('',#17944,#3730);
#2981=LINE('',#17946,#3731);
#2982=LINE('',#17948,#3732);
#2983=LINE('',#17950,#3733);
#2984=LINE('',#17952,#3734);
#2985=LINE('',#17955,#3735);
#2986=LINE('',#17957,#3736);
#2987=LINE('',#17959,#3737);
#2988=LINE('',#17961,#3738);
#2989=LINE('',#17963,#3739);
#2990=LINE('',#17965,#3740);
#2991=LINE('',#17967,#3741);
#2992=LINE('',#17970,#3742);
#2993=LINE('',#17972,#3743);
#3685=VECTOR('',#12198,1000.);
#3686=VECTOR('',#12201,1000.);
#3687=VECTOR('',#12208,1000.);
#3688=VECTOR('',#12211,1000.);
#3689=VECTOR('',#12214,1000.);
#3690=VECTOR('',#12215,1000.);
#3691=VECTOR('',#12216,1000.);
#3692=VECTOR('',#12219,1000.);
#3693=VECTOR('',#12220,1000.);
#3694=VECTOR('',#12221,1000.);
#3695=VECTOR('',#12224,1000.);
#3696=VECTOR('',#12225,1000.);
#3697=VECTOR('',#12226,1000.);
#3698=VECTOR('',#12227,1000.);
#3699=VECTOR('',#12228,1000.);
#3700=VECTOR('',#12229,1000.);
#3701=VECTOR('',#12230,1000.);
#3702=VECTOR('',#12231,1000.);
#3703=VECTOR('',#12232,1000.);
#3704=VECTOR('',#12233,1000.);
#3705=VECTOR('',#12234,1000.);
#3706=VECTOR('',#12235,1000.);
#3707=VECTOR('',#12236,1000.);
#3708=VECTOR('',#12237,1000.);
#3709=VECTOR('',#12238,1000.);
#3710=VECTOR('',#12239,1000.);
#3711=VECTOR('',#12244,1000.);
#3712=VECTOR('',#12245,1000.);
#3713=VECTOR('',#12246,1000.);
#3714=VECTOR('',#12247,1000.);
#3715=VECTOR('',#12248,1000.);
#3716=VECTOR('',#12249,1000.);
#3717=VECTOR('',#12250,1000.);
#3718=VECTOR('',#12251,1000.);
#3719=VECTOR('',#12252,1000.);
#3720=VECTOR('',#12253,1000.);
#3721=VECTOR('',#12254,1000.);
#3722=VECTOR('',#12255,1000.);
#3723=VECTOR('',#12256,1000.);
#3724=VECTOR('',#12257,1000.);
#3725=VECTOR('',#12258,1000.);
#3726=VECTOR('',#12259,1000.);
#3727=VECTOR('',#12266,3.);
#3728=VECTOR('',#12273,1000.);
#3729=VECTOR('',#12276,1000.);
#3730=VECTOR('',#12279,1000.);
#3731=VECTOR('',#12282,1000.);
#3732=VECTOR('',#12285,1000.);
#3733=VECTOR('',#12288,1000.);
#3734=VECTOR('',#12291,1000.);
#3735=VECTOR('',#12296,1000.);
#3736=VECTOR('',#12299,1000.);
#3737=VECTOR('',#12302,1000.);
#3738=VECTOR('',#12305,1000.);
#3739=VECTOR('',#12308,1000.);
#3740=VECTOR('',#12311,1000.);
#3741=VECTOR('',#12314,1000.);
#3742=VECTOR('',#12319,3.5);
#3743=VECTOR('',#12322,3.);
#4430=VERTEX_POINT('',#17836);
#4431=VERTEX_POINT('',#17837);
#4432=VERTEX_POINT('',#17839);
#4433=VERTEX_POINT('',#17841);
#4434=VERTEX_POINT('',#17845);
#4435=VERTEX_POINT('',#17846);
#4436=VERTEX_POINT('',#17848);
#4437=VERTEX_POINT('',#17850);
#4438=VERTEX_POINT('',#17854);
#4439=VERTEX_POINT('',#17856);
#4440=VERTEX_POINT('',#17860);
#4441=VERTEX_POINT('',#17862);
#4442=VERTEX_POINT('',#17866);
#4443=VERTEX_POINT('',#17868);
#4444=VERTEX_POINT('',#17870);
#4445=VERTEX_POINT('',#17872);
#4446=VERTEX_POINT('',#17874);
#4447=VERTEX_POINT('',#17876);
#4448=VERTEX_POINT('',#17878);
#4449=VERTEX_POINT('',#17881);
#4450=VERTEX_POINT('',#17883);
#4451=VERTEX_POINT('',#17885);
#4452=VERTEX_POINT('',#17887);
#4453=VERTEX_POINT('',#17889);
#4454=VERTEX_POINT('',#17891);
#4455=VERTEX_POINT('',#17893);
#4456=VERTEX_POINT('',#17896);
#4457=VERTEX_POINT('',#17899);
#4458=VERTEX_POINT('',#17901);
#4459=VERTEX_POINT('',#17903);
#4460=VERTEX_POINT('',#17905);
#4461=VERTEX_POINT('',#17907);
#4462=VERTEX_POINT('',#17909);
#4463=VERTEX_POINT('',#17911);
#4464=VERTEX_POINT('',#17914);
#4465=VERTEX_POINT('',#17916);
#4466=VERTEX_POINT('',#17918);
#4467=VERTEX_POINT('',#17920);
#4468=VERTEX_POINT('',#17922);
#4469=VERTEX_POINT('',#17924);
#4470=VERTEX_POINT('',#17926);
#4471=VERTEX_POINT('',#17929);
#4472=VERTEX_POINT('',#17932);
#4473=VERTEX_POINT('',#17933);
#4474=VERTEX_POINT('',#17935);
#5530=EDGE_CURVE('',#4430,#4431,#2935,.T.);
#5531=EDGE_CURVE('',#4431,#4432,#2344,.T.);
#5532=EDGE_CURVE('',#4433,#4432,#2936,.T.);
#5533=EDGE_CURVE('',#4430,#4433,#2345,.T.);
#5534=EDGE_CURVE('',#4434,#4435,#2346,.T.);
#5535=EDGE_CURVE('',#4436,#4434,#2937,.T.);
#5536=EDGE_CURVE('',#4436,#4437,#2347,.T.);
#5537=EDGE_CURVE('',#4437,#4435,#2938,.T.);
#5538=EDGE_CURVE('',#4434,#4438,#2939,.T.);
#5539=EDGE_CURVE('',#4439,#4438,#2940,.T.);
#5540=EDGE_CURVE('',#4436,#4439,#2941,.T.);
#5541=EDGE_CURVE('',#4440,#4435,#2942,.T.);
#5542=EDGE_CURVE('',#4441,#4437,#2943,.T.);
#5543=EDGE_CURVE('',#4441,#4440,#2944,.T.);
#5544=EDGE_CURVE('',#4439,#4442,#2945,.T.);
#5545=EDGE_CURVE('',#4442,#4443,#2946,.T.);
#5546=EDGE_CURVE('',#4443,#4444,#2947,.T.);
#5547=EDGE_CURVE('',#4444,#4445,#2948,.T.);
#5548=EDGE_CURVE('',#4445,#4446,#2949,.T.);
#5549=EDGE_CURVE('',#4446,#4447,#2950,.T.);
#5550=EDGE_CURVE('',#4447,#4448,#2951,.T.);
#5551=EDGE_CURVE('',#4448,#4430,#2952,.T.);
#5552=EDGE_CURVE('',#4449,#4433,#2953,.T.);
#5553=EDGE_CURVE('',#4450,#4449,#2954,.T.);
#5554=EDGE_CURVE('',#4451,#4450,#2955,.T.);
#5555=EDGE_CURVE('',#4452,#4451,#2956,.T.);
#5556=EDGE_CURVE('',#4453,#4452,#2957,.T.);
#5557=EDGE_CURVE('',#4454,#4453,#2958,.T.);
#5558=EDGE_CURVE('',#4455,#4454,#2959,.T.);
#5559=EDGE_CURVE('',#4441,#4455,#2960,.T.);
#5560=EDGE_CURVE('',#4456,#4456,#2348,.T.);
#5561=EDGE_CURVE('',#4440,#4457,#2961,.T.);
#5562=EDGE_CURVE('',#4457,#4458,#2962,.T.);
#5563=EDGE_CURVE('',#4458,#4459,#2963,.T.);
#5564=EDGE_CURVE('',#4459,#4460,#2964,.T.);
#5565=EDGE_CURVE('',#4460,#4461,#2965,.T.);
#5566=EDGE_CURVE('',#4461,#4462,#2966,.T.);
#5567=EDGE_CURVE('',#4462,#4463,#2967,.T.);
#5568=EDGE_CURVE('',#4463,#4432,#2968,.T.);
#5569=EDGE_CURVE('',#4464,#4431,#2969,.T.);
#5570=EDGE_CURVE('',#4465,#4464,#2970,.T.);
#5571=EDGE_CURVE('',#4466,#4465,#2971,.T.);
#5572=EDGE_CURVE('',#4467,#4466,#2972,.T.);
#5573=EDGE_CURVE('',#4468,#4467,#2973,.T.);
#5574=EDGE_CURVE('',#4469,#4468,#2974,.T.);
#5575=EDGE_CURVE('',#4470,#4469,#2975,.T.);
#5576=EDGE_CURVE('',#4438,#4470,#2976,.T.);
#5577=EDGE_CURVE('',#4471,#4471,#2349,.T.);
#5578=EDGE_CURVE('',#4472,#4473,#2350,.T.);
#5579=EDGE_CURVE('',#4473,#4474,#2977,.T.);
#5580=EDGE_CURVE('',#4474,#4474,#2351,.T.);
#5581=EDGE_CURVE('',#4473,#4472,#2352,.T.);
#5582=EDGE_CURVE('',#4455,#4457,#2978,.T.);
#5583=EDGE_CURVE('',#4454,#4458,#2979,.T.);
#5584=EDGE_CURVE('',#4453,#4459,#2980,.T.);
#5585=EDGE_CURVE('',#4452,#4460,#2981,.T.);
#5586=EDGE_CURVE('',#4451,#4461,#2982,.T.);
#5587=EDGE_CURVE('',#4450,#4462,#2983,.T.);
#5588=EDGE_CURVE('',#4449,#4463,#2984,.T.);
#5589=EDGE_CURVE('',#4442,#4470,#2985,.T.);
#5590=EDGE_CURVE('',#4443,#4469,#2986,.T.);
#5591=EDGE_CURVE('',#4444,#4468,#2987,.T.);
#5592=EDGE_CURVE('',#4445,#4467,#2988,.T.);
#5593=EDGE_CURVE('',#4446,#4466,#2989,.T.);
#5594=EDGE_CURVE('',#4447,#4465,#2990,.T.);
#5595=EDGE_CURVE('',#4448,#4464,#2991,.T.);
#5596=EDGE_CURVE('',#4472,#4471,#2992,.T.);
#5597=EDGE_CURVE('',#4474,#4456,#2993,.T.);
#7434=ORIENTED_EDGE('',*,*,#5530,.T.);
#7435=ORIENTED_EDGE('',*,*,#5531,.T.);
#7436=ORIENTED_EDGE('',*,*,#5532,.F.);
#7437=ORIENTED_EDGE('',*,*,#5533,.F.);
#7438=ORIENTED_EDGE('',*,*,#5534,.F.);
#7439=ORIENTED_EDGE('',*,*,#5535,.F.);
#7440=ORIENTED_EDGE('',*,*,#5536,.T.);
#7441=ORIENTED_EDGE('',*,*,#5537,.T.);
#7442=ORIENTED_EDGE('',*,*,#5538,.T.);
#7443=ORIENTED_EDGE('',*,*,#5539,.F.);
#7444=ORIENTED_EDGE('',*,*,#5540,.F.);
#7445=ORIENTED_EDGE('',*,*,#5535,.T.);
#7446=ORIENTED_EDGE('',*,*,#5541,.T.);
#7447=ORIENTED_EDGE('',*,*,#5537,.F.);
#7448=ORIENTED_EDGE('',*,*,#5542,.F.);
#7449=ORIENTED_EDGE('',*,*,#5543,.T.);
#7450=ORIENTED_EDGE('',*,*,#5536,.F.);
#7451=ORIENTED_EDGE('',*,*,#5540,.T.);
#7452=ORIENTED_EDGE('',*,*,#5544,.T.);
#7453=ORIENTED_EDGE('',*,*,#5545,.T.);
#7454=ORIENTED_EDGE('',*,*,#5546,.T.);
#7455=ORIENTED_EDGE('',*,*,#5547,.T.);
#7456=ORIENTED_EDGE('',*,*,#5548,.T.);
#7457=ORIENTED_EDGE('',*,*,#5549,.T.);
#7458=ORIENTED_EDGE('',*,*,#5550,.T.);
#7459=ORIENTED_EDGE('',*,*,#5551,.T.);
#7460=ORIENTED_EDGE('',*,*,#5533,.T.);
#7461=ORIENTED_EDGE('',*,*,#5552,.F.);
#7462=ORIENTED_EDGE('',*,*,#5553,.F.);
#7463=ORIENTED_EDGE('',*,*,#5554,.F.);
#7464=ORIENTED_EDGE('',*,*,#5555,.F.);
#7465=ORIENTED_EDGE('',*,*,#5556,.F.);
#7466=ORIENTED_EDGE('',*,*,#5557,.F.);
#7467=ORIENTED_EDGE('',*,*,#5558,.F.);
#7468=ORIENTED_EDGE('',*,*,#5559,.F.);
#7469=ORIENTED_EDGE('',*,*,#5542,.T.);
#7470=ORIENTED_EDGE('',*,*,#5560,.T.);
#7471=ORIENTED_EDGE('',*,*,#5534,.T.);
#7472=ORIENTED_EDGE('',*,*,#5541,.F.);
#7473=ORIENTED_EDGE('',*,*,#5561,.T.);
#7474=ORIENTED_EDGE('',*,*,#5562,.T.);
#7475=ORIENTED_EDGE('',*,*,#5563,.T.);
#7476=ORIENTED_EDGE('',*,*,#5564,.T.);
#7477=ORIENTED_EDGE('',*,*,#5565,.T.);
#7478=ORIENTED_EDGE('',*,*,#5566,.T.);
#7479=ORIENTED_EDGE('',*,*,#5567,.T.);
#7480=ORIENTED_EDGE('',*,*,#5568,.T.);
#7481=ORIENTED_EDGE('',*,*,#5531,.F.);
#7482=ORIENTED_EDGE('',*,*,#5569,.F.);
#7483=ORIENTED_EDGE('',*,*,#5570,.F.);
#7484=ORIENTED_EDGE('',*,*,#5571,.F.);
#7485=ORIENTED_EDGE('',*,*,#5572,.F.);
#7486=ORIENTED_EDGE('',*,*,#5573,.F.);
#7487=ORIENTED_EDGE('',*,*,#5574,.F.);
#7488=ORIENTED_EDGE('',*,*,#5575,.F.);
#7489=ORIENTED_EDGE('',*,*,#5576,.F.);
#7490=ORIENTED_EDGE('',*,*,#5538,.F.);
#7491=ORIENTED_EDGE('',*,*,#5577,.T.);
#7492=ORIENTED_EDGE('',*,*,#5578,.T.);
#7493=ORIENTED_EDGE('',*,*,#5579,.T.);
#7494=ORIENTED_EDGE('',*,*,#5580,.T.);
#7495=ORIENTED_EDGE('',*,*,#5579,.F.);
#7496=ORIENTED_EDGE('',*,*,#5581,.T.);
#7497=ORIENTED_EDGE('',*,*,#5561,.F.);
#7498=ORIENTED_EDGE('',*,*,#5543,.F.);
#7499=ORIENTED_EDGE('',*,*,#5559,.T.);
#7500=ORIENTED_EDGE('',*,*,#5582,.T.);
#7501=ORIENTED_EDGE('',*,*,#5562,.F.);
#7502=ORIENTED_EDGE('',*,*,#5582,.F.);
#7503=ORIENTED_EDGE('',*,*,#5558,.T.);
#7504=ORIENTED_EDGE('',*,*,#5583,.T.);
#7505=ORIENTED_EDGE('',*,*,#5563,.F.);
#7506=ORIENTED_EDGE('',*,*,#5583,.F.);
#7507=ORIENTED_EDGE('',*,*,#5557,.T.);
#7508=ORIENTED_EDGE('',*,*,#5584,.T.);
#7509=ORIENTED_EDGE('',*,*,#5564,.F.);
#7510=ORIENTED_EDGE('',*,*,#5584,.F.);
#7511=ORIENTED_EDGE('',*,*,#5556,.T.);
#7512=ORIENTED_EDGE('',*,*,#5585,.T.);
#7513=ORIENTED_EDGE('',*,*,#5565,.F.);
#7514=ORIENTED_EDGE('',*,*,#5585,.F.);
#7515=ORIENTED_EDGE('',*,*,#5555,.T.);
#7516=ORIENTED_EDGE('',*,*,#5586,.T.);
#7517=ORIENTED_EDGE('',*,*,#5566,.F.);
#7518=ORIENTED_EDGE('',*,*,#5586,.F.);
#7519=ORIENTED_EDGE('',*,*,#5554,.T.);
#7520=ORIENTED_EDGE('',*,*,#5587,.T.);
#7521=ORIENTED_EDGE('',*,*,#5567,.F.);
#7522=ORIENTED_EDGE('',*,*,#5587,.F.);
#7523=ORIENTED_EDGE('',*,*,#5553,.T.);
#7524=ORIENTED_EDGE('',*,*,#5588,.T.);
#7525=ORIENTED_EDGE('',*,*,#5568,.F.);
#7526=ORIENTED_EDGE('',*,*,#5588,.F.);
#7527=ORIENTED_EDGE('',*,*,#5552,.T.);
#7528=ORIENTED_EDGE('',*,*,#5532,.T.);
#7529=ORIENTED_EDGE('',*,*,#5576,.T.);
#7530=ORIENTED_EDGE('',*,*,#5589,.F.);
#7531=ORIENTED_EDGE('',*,*,#5544,.F.);
#7532=ORIENTED_EDGE('',*,*,#5539,.T.);
#7533=ORIENTED_EDGE('',*,*,#5575,.T.);
#7534=ORIENTED_EDGE('',*,*,#5590,.F.);
#7535=ORIENTED_EDGE('',*,*,#5545,.F.);
#7536=ORIENTED_EDGE('',*,*,#5589,.T.);
#7537=ORIENTED_EDGE('',*,*,#5574,.T.);
#7538=ORIENTED_EDGE('',*,*,#5591,.F.);
#7539=ORIENTED_EDGE('',*,*,#5546,.F.);
#7540=ORIENTED_EDGE('',*,*,#5590,.T.);
#7541=ORIENTED_EDGE('',*,*,#5573,.T.);
#7542=ORIENTED_EDGE('',*,*,#5592,.F.);
#7543=ORIENTED_EDGE('',*,*,#5547,.F.);
#7544=ORIENTED_EDGE('',*,*,#5591,.T.);
#7545=ORIENTED_EDGE('',*,*,#5572,.T.);
#7546=ORIENTED_EDGE('',*,*,#5593,.F.);
#7547=ORIENTED_EDGE('',*,*,#5548,.F.);
#7548=ORIENTED_EDGE('',*,*,#5592,.T.);
#7549=ORIENTED_EDGE('',*,*,#5571,.T.);
#7550=ORIENTED_EDGE('',*,*,#5594,.F.);
#7551=ORIENTED_EDGE('',*,*,#5549,.F.);
#7552=ORIENTED_EDGE('',*,*,#5593,.T.);
#7553=ORIENTED_EDGE('',*,*,#5570,.T.);
#7554=ORIENTED_EDGE('',*,*,#5595,.F.);
#7555=ORIENTED_EDGE('',*,*,#5550,.F.);
#7556=ORIENTED_EDGE('',*,*,#5594,.T.);
#7557=ORIENTED_EDGE('',*,*,#5569,.T.);
#7558=ORIENTED_EDGE('',*,*,#5530,.F.);
#7559=ORIENTED_EDGE('',*,*,#5551,.F.);
#7560=ORIENTED_EDGE('',*,*,#5595,.T.);
#7561=ORIENTED_EDGE('',*,*,#5578,.F.);
#7562=ORIENTED_EDGE('',*,*,#5596,.T.);
#7563=ORIENTED_EDGE('',*,*,#5577,.F.);
#7564=ORIENTED_EDGE('',*,*,#5596,.F.);
#7565=ORIENTED_EDGE('',*,*,#5581,.F.);
#7566=ORIENTED_EDGE('',*,*,#5580,.F.);
#7567=ORIENTED_EDGE('',*,*,#5597,.T.);
#7568=ORIENTED_EDGE('',*,*,#5560,.F.);
#7569=ORIENTED_EDGE('',*,*,#5597,.F.);
#9276=CYLINDRICAL_SURFACE('',#10581,17.1);
#9277=CYLINDRICAL_SURFACE('',#10584,9.);
#9278=CYLINDRICAL_SURFACE('',#10593,3.);
#9574=ADVANCED_FACE('',(#1208),#9276,.T.);
#9575=ADVANCED_FACE('',(#1209),#9277,.F.);
#9576=ADVANCED_FACE('',(#1210),#865,.F.);
#9577=ADVANCED_FACE('',(#1211),#866,.F.);
#9578=ADVANCED_FACE('',(#1212,#491),#867,.T.);
#9579=ADVANCED_FACE('',(#1213,#492),#868,.F.);
#9580=ADVANCED_FACE('',(#1214),#9278,.F.);
#9581=ADVANCED_FACE('',(#1215),#869,.T.);
#9582=ADVANCED_FACE('',(#1216),#870,.T.);
#9583=ADVANCED_FACE('',(#1217),#871,.T.);
#9584=ADVANCED_FACE('',(#1218),#872,.T.);
#9585=ADVANCED_FACE('',(#1219),#873,.T.);
#9586=ADVANCED_FACE('',(#1220),#874,.T.);
#9587=ADVANCED_FACE('',(#1221),#875,.T.);
#9588=ADVANCED_FACE('',(#1222),#876,.T.);
#9589=ADVANCED_FACE('',(#1223),#877,.F.);
#9590=ADVANCED_FACE('',(#1224),#878,.F.);
#9591=ADVANCED_FACE('',(#1225),#879,.F.);
#9592=ADVANCED_FACE('',(#1226),#880,.F.);
#9593=ADVANCED_FACE('',(#1227),#881,.F.);
#9594=ADVANCED_FACE('',(#1228),#882,.F.);
#9595=ADVANCED_FACE('',(#1229),#883,.F.);
#9596=ADVANCED_FACE('',(#1230),#884,.F.);
#9597=ADVANCED_FACE('',(#1231),#349,.F.);
#9598=ADVANCED_FACE('',(#1232),#350,.F.);
#9944=CLOSED_SHELL('',(#9574,#9575,#9576,#9577,#9578,#9579,#9580,#9581,
#9582,#9583,#9584,#9585,#9586,#9587,#9588,#9589,#9590,#9591,#9592,#9593,
#9594,#9595,#9596,#9597,#9598));
#10580=AXIS2_PLACEMENT_3D('',#17834,#12194,#12195);
#10581=AXIS2_PLACEMENT_3D('',#17835,#12196,#12197);
#10582=AXIS2_PLACEMENT_3D('',#17840,#12199,#12200);
#10583=AXIS2_PLACEMENT_3D('',#17843,#12202,#12203);
#10584=AXIS2_PLACEMENT_3D('',#17844,#12204,#12205);
#10585=AXIS2_PLACEMENT_3D('',#17847,#12206,#12207);
#10586=AXIS2_PLACEMENT_3D('',#17851,#12209,#12210);
#10587=AXIS2_PLACEMENT_3D('',#17853,#12212,#12213);
#10588=AXIS2_PLACEMENT_3D('',#17859,#12217,#12218);
#10589=AXIS2_PLACEMENT_3D('',#17865,#12222,#12223);
#10590=AXIS2_PLACEMENT_3D('',#17897,#12240,#12241);
#10591=AXIS2_PLACEMENT_3D('',#17898,#12242,#12243);
#10592=AXIS2_PLACEMENT_3D('',#17930,#12260,#12261);
#10593=AXIS2_PLACEMENT_3D('',#17931,#12262,#12263);
#10594=AXIS2_PLACEMENT_3D('',#17934,#12264,#12265);
#10595=AXIS2_PLACEMENT_3D('',#17937,#12267,#12268);
#10596=AXIS2_PLACEMENT_3D('',#17938,#12269,#12270);
#10597=AXIS2_PLACEMENT_3D('',#17939,#12271,#12272);
#10598=AXIS2_PLACEMENT_3D('',#17941,#12274,#12275);
#10599=AXIS2_PLACEMENT_3D('',#17943,#12277,#12278);
#10600=AXIS2_PLACEMENT_3D('',#17945,#12280,#12281);
#10601=AXIS2_PLACEMENT_3D('',#17947,#12283,#12284);
#10602=AXIS2_PLACEMENT_3D('',#17949,#12286,#12287);
#10603=AXIS2_PLACEMENT_3D('',#17951,#12289,#12290);
#10604=AXIS2_PLACEMENT_3D('',#17953,#12292,#12293);
#10605=AXIS2_PLACEMENT_3D('',#17954,#12294,#12295);
#10606=AXIS2_PLACEMENT_3D('',#17956,#12297,#12298);
#10607=AXIS2_PLACEMENT_3D('',#17958,#12300,#12301);
#10608=AXIS2_PLACEMENT_3D('',#17960,#12303,#12304);
#10609=AXIS2_PLACEMENT_3D('',#17962,#12306,#12307);
#10610=AXIS2_PLACEMENT_3D('',#17964,#12309,#12310);
#10611=AXIS2_PLACEMENT_3D('',#17966,#12312,#12313);
#10612=AXIS2_PLACEMENT_3D('',#17968,#12315,#12316);
#10613=AXIS2_PLACEMENT_3D('',#17969,#12317,#12318);
#10614=AXIS2_PLACEMENT_3D('',#17971,#12320,#12321);
#12194=DIRECTION('axis',(0.,0.,1.));
#12195=DIRECTION('refdir',(1.,0.,0.));
#12196=DIRECTION('center_axis',(0.,-1.,0.));
#12197=DIRECTION('ref_axis',(0.,0.,-1.));
#12198=DIRECTION('',(0.,-1.,0.));
#12199=DIRECTION('center_axis',(0.,1.,0.));
#12200=DIRECTION('ref_axis',(0.,0.,1.));
#12201=DIRECTION('',(0.,-1.,0.));
#12202=DIRECTION('center_axis',(0.,1.,0.));
#12203=DIRECTION('ref_axis',(0.,0.,1.));
#12204=DIRECTION('center_axis',(0.,-1.,0.));
#12205=DIRECTION('ref_axis',(0.,0.,-1.));
#12206=DIRECTION('center_axis',(0.,1.,0.));
#12207=DIRECTION('ref_axis',(0.,0.,1.));
#12208=DIRECTION('',(0.,-1.,0.));
#12209=DIRECTION('center_axis',(0.,1.,0.));
#12210=DIRECTION('ref_axis',(0.,0.,1.));
#12211=DIRECTION('',(0.,-1.,0.));
#12212=DIRECTION('center_axis',(-0.158158067254484,0.,-0.987413806750912));
#12213=DIRECTION('ref_axis',(-0.987413806750912,0.,0.158158067254484));
#12214=DIRECTION('',(0.987413806750912,0.,-0.158158067254484));
#12215=DIRECTION('',(0.,-1.,0.));
#12216=DIRECTION('',(0.987413806750912,0.,-0.158158067254484));
#12217=DIRECTION('center_axis',(0.158158067254484,0.,-0.987413806750912));
#12218=DIRECTION('ref_axis',(-0.987413806750912,0.,-0.158158067254484));
#12219=DIRECTION('',(0.987413806750912,0.,0.158158067254484));
#12220=DIRECTION('',(0.987413806750912,0.,0.158158067254484));
#12221=DIRECTION('',(0.,-1.,0.));
#12222=DIRECTION('center_axis',(0.,1.,0.));
#12223=DIRECTION('ref_axis',(0.,0.,1.));
#12224=DIRECTION('',(0.392864972480271,0.,-0.919596168651259));
#12225=DIRECTION('',(-0.971825883503931,0.,-0.235699919711066));
#12226=DIRECTION('',(0.238761369565624,0.,-0.971078270997321));
#12227=DIRECTION('',(-0.997167509069151,0.,-0.0752127572744475));
#12228=DIRECTION('',(0.0783548658721971,0.,-0.996925531318237));
#12229=DIRECTION('',(-0.996185580363772,0.,0.0872598961453321));
#12230=DIRECTION('',(-0.0841200752155391,0.,-0.996455625176421));
#12231=DIRECTION('',(-0.968906018663139,0.,0.247429034267092));
#12232=DIRECTION('',(0.968906018663139,0.,0.247429034267092));
#12233=DIRECTION('',(0.0841200752155391,0.,-0.996455625176421));
#12234=DIRECTION('',(0.996185580363772,0.,0.0872598961453321));
#12235=DIRECTION('',(-0.0783548658721971,0.,-0.996925531318237));
#12236=DIRECTION('',(0.997167509069151,0.,-0.0752127572744475));
#12237=DIRECTION('',(-0.238761369565624,0.,-0.971078270997321));
#12238=DIRECTION('',(0.971825883503931,0.,-0.235699919711066));
#12239=DIRECTION('',(-0.392864972480271,0.,-0.919596168651259));
#12240=DIRECTION('center_axis',(0.,-1.,0.));
#12241=DIRECTION('ref_axis',(0.,0.,1.));
#12242=DIRECTION('center_axis',(0.,1.,0.));
#12243=DIRECTION('ref_axis',(0.,0.,1.));
#12244=DIRECTION('',(-0.392864972480271,0.,-0.919596168651259));
#12245=DIRECTION('',(0.971825883503931,0.,-0.235699919711066));
#12246=DIRECTION('',(-0.238761369565624,0.,-0.971078270997321));
#12247=DIRECTION('',(0.997167509069151,0.,-0.0752127572744475));
#12248=DIRECTION('',(-0.0783548658721971,0.,-0.996925531318237));
#12249=DIRECTION('',(0.996185580363772,0.,0.0872598961453321));
#12250=DIRECTION('',(0.0841200752155391,0.,-0.996455625176421));
#12251=DIRECTION('',(0.968906018663139,0.,0.247429034267092));
#12252=DIRECTION('',(-0.968906018663139,0.,0.247429034267092));
#12253=DIRECTION('',(-0.0841200752155391,0.,-0.996455625176421));
#12254=DIRECTION('',(-0.996185580363772,0.,0.0872598961453321));
#12255=DIRECTION('',(0.0783548658721971,0.,-0.996925531318237));
#12256=DIRECTION('',(-0.997167509069151,0.,-0.0752127572744475));
#12257=DIRECTION('',(0.238761369565624,0.,-0.971078270997321));
#12258=DIRECTION('',(-0.971825883503931,0.,-0.235699919711066));
#12259=DIRECTION('',(0.392864972480271,0.,-0.919596168651259));
#12260=DIRECTION('center_axis',(0.,1.,0.));
#12261=DIRECTION('ref_axis',(0.,0.,1.));
#12262=DIRECTION('center_axis',(0.,1.,0.));
#12263=DIRECTION('ref_axis',(0.,0.,1.));
#12264=DIRECTION('center_axis',(0.,-1.,0.));
#12265=DIRECTION('ref_axis',(0.,0.,1.));
#12266=DIRECTION('',(0.,1.,0.));
#12267=DIRECTION('center_axis',(0.,1.,0.));
#12268=DIRECTION('ref_axis',(0.,0.,1.));
#12269=DIRECTION('center_axis',(0.,-1.,0.));
#12270=DIRECTION('ref_axis',(0.,0.,1.));
#12271=DIRECTION('center_axis',(-0.91959616865126,0.,0.392864972480271));
#12272=DIRECTION('ref_axis',(0.392864972480271,0.,0.91959616865126));
#12273=DIRECTION('',(0.,-1.,0.));
#12274=DIRECTION('center_axis',(-0.235699919711066,0.,-0.971825883503932));
#12275=DIRECTION('ref_axis',(-0.971825883503932,0.,0.235699919711066));
#12276=DIRECTION('',(0.,-1.,0.));
#12277=DIRECTION('center_axis',(-0.971078270997322,0.,0.238761369565624));
#12278=DIRECTION('ref_axis',(0.238761369565624,0.,0.971078270997322));
#12279=DIRECTION('',(0.,-1.,0.));
#12280=DIRECTION('center_axis',(-0.0752127572744475,0.,-0.997167509069151));
#12281=DIRECTION('ref_axis',(-0.997167509069151,0.,0.0752127572744475));
#12282=DIRECTION('',(0.,-1.,0.));
#12283=DIRECTION('center_axis',(-0.996925531318237,0.,0.0783548658721971));
#12284=DIRECTION('ref_axis',(0.0783548658721971,0.,0.996925531318237));
#12285=DIRECTION('',(0.,-1.,0.));
#12286=DIRECTION('center_axis',(0.0872598961453321,0.,-0.996185580363772));
#12287=DIRECTION('ref_axis',(-0.996185580363772,0.,-0.0872598961453321));
#12288=DIRECTION('',(0.,-1.,0.));
#12289=DIRECTION('center_axis',(-0.996455625176421,0.,-0.0841200752155391));
#12290=DIRECTION('ref_axis',(-0.0841200752155391,0.,0.996455625176421));
#12291=DIRECTION('',(0.,-1.,0.));
#12292=DIRECTION('center_axis',(0.247429034267092,0.,-0.968906018663139));
#12293=DIRECTION('ref_axis',(-0.968906018663139,0.,-0.247429034267092));
#12294=DIRECTION('center_axis',(-0.91959616865126,0.,-0.392864972480271));
#12295=DIRECTION('ref_axis',(-0.392864972480271,0.,0.91959616865126));
#12296=DIRECTION('',(0.,-1.,0.));
#12297=DIRECTION('center_axis',(-0.235699919711066,0.,0.971825883503932));
#12298=DIRECTION('ref_axis',(0.971825883503932,0.,0.235699919711066));
#12299=DIRECTION('',(0.,-1.,0.));
#12300=DIRECTION('center_axis',(-0.971078270997322,0.,-0.238761369565624));
#12301=DIRECTION('ref_axis',(-0.238761369565624,0.,0.971078270997322));
#12302=DIRECTION('',(0.,-1.,0.));
#12303=DIRECTION('center_axis',(-0.0752127572744475,0.,0.997167509069151));
#12304=DIRECTION('ref_axis',(0.997167509069151,0.,0.0752127572744475));
#12305=DIRECTION('',(0.,-1.,0.));
#12306=DIRECTION('center_axis',(-0.996925531318237,0.,-0.0783548658721971));
#12307=DIRECTION('ref_axis',(-0.0783548658721971,0.,0.996925531318237));
#12308=DIRECTION('',(0.,-1.,0.));
#12309=DIRECTION('center_axis',(0.0872598961453321,0.,0.996185580363772));
#12310=DIRECTION('ref_axis',(0.996185580363772,0.,-0.0872598961453321));
#12311=DIRECTION('',(0.,-1.,0.));
#12312=DIRECTION('center_axis',(-0.996455625176421,0.,0.0841200752155391));
#12313=DIRECTION('ref_axis',(0.0841200752155391,0.,0.996455625176421));
#12314=DIRECTION('',(0.,-1.,0.));
#12315=DIRECTION('center_axis',(0.247429034267092,0.,0.968906018663139));
#12316=DIRECTION('ref_axis',(0.968906018663139,0.,-0.247429034267092));
#12317=DIRECTION('center_axis',(0.,-1.,0.));
#12318=DIRECTION('ref_axis',(0.,0.,-1.));
#12319=DIRECTION('',(-8.65956056235489E-17,-0.707106781186551,0.707106781186544));
#12320=DIRECTION('center_axis',(0.,1.,0.));
#12321=DIRECTION('ref_axis',(0.,0.,1.));
#12322=DIRECTION('',(-8.65956056235494E-17,0.707106781186546,-0.707106781186549));
#17834=CARTESIAN_POINT('',(0.,0.,0.));
#17835=CARTESIAN_POINT('Origin',(0.,4.,-3.1));
#17836=CARTESIAN_POINT('',(8.7469213123627,4.,-17.7935825296398));
#17837=CARTESIAN_POINT('',(8.7469213123627,-4.,-17.7935825296398));
#17838=CARTESIAN_POINT('',(8.7469213123627,4.,-17.7935825296398));
#17839=CARTESIAN_POINT('',(-8.7469213123627,-4.,-17.7935825296398));
#17840=CARTESIAN_POINT('Origin',(0.,-4.,-3.1));
#17841=CARTESIAN_POINT('',(-8.7469213123627,4.,-17.7935825296398));
#17842=CARTESIAN_POINT('',(-8.7469213123627,4.,-17.7935825296398));
#17843=CARTESIAN_POINT('Origin',(0.,4.,-3.1));
#17844=CARTESIAN_POINT('Origin',(0.,4.,0.));
#17845=CARTESIAN_POINT('',(4.6593991028887,-4.,-7.7));
#17846=CARTESIAN_POINT('',(-4.6593991028887,-4.,-7.7));
#17847=CARTESIAN_POINT('Origin',(0.,-4.,0.));
#17848=CARTESIAN_POINT('',(4.6593991028887,4.,-7.7));
#17849=CARTESIAN_POINT('',(4.6593991028887,4.,-7.7));
#17850=CARTESIAN_POINT('',(-4.6593991028887,4.,-7.7));
#17851=CARTESIAN_POINT('Origin',(0.,4.,0.));
#17852=CARTESIAN_POINT('',(-4.6593991028887,4.,-7.7));
#17853=CARTESIAN_POINT('Origin',(4.6593991028887,4.,-7.7));
#17854=CARTESIAN_POINT('',(15.8596026089922,-4.,-9.49398194279967));
#17855=CARTESIAN_POINT('',(4.6593991028887,-4.,-7.7));
#17856=CARTESIAN_POINT('',(15.8596026089922,4.,-9.49398194279967));
#17857=CARTESIAN_POINT('',(15.8596026089922,4.,-9.49398194279967));
#17858=CARTESIAN_POINT('',(4.6593991028887,4.,-7.7));
#17859=CARTESIAN_POINT('Origin',(-15.8596026089922,4.,-9.49398194279967));
#17860=CARTESIAN_POINT('',(-15.8596026089922,-4.,-9.49398194279967));
#17861=CARTESIAN_POINT('',(-15.8596026089922,-4.,-9.49398194279967));
#17862=CARTESIAN_POINT('',(-15.8596026089922,4.,-9.49398194279967));
#17863=CARTESIAN_POINT('',(-15.8596026089922,4.,-9.49398194279967));
#17864=CARTESIAN_POINT('',(-15.8596026089922,4.,-9.49398194279967));
#17865=CARTESIAN_POINT('Origin',(0.,4.,0.));
#17866=CARTESIAN_POINT('',(16.7042622998248,4.,-11.4711137053999));
#17867=CARTESIAN_POINT('',(9.98182727519893,4.,4.26438303187517));
#17868=CARTESIAN_POINT('',(14.6148366502913,4.,-11.9778685327787));
#17869=CARTESIAN_POINT('',(3.55556121796803,4.,-14.6601086086066));
#17870=CARTESIAN_POINT('',(15.1281735948574,4.,-14.0656868154229));
#17871=CARTESIAN_POINT('',(11.0045483578897,4.,2.7057149931719));
#17872=CARTESIAN_POINT('',(12.9842634503587,4.,-14.227394243563));
#17873=CARTESIAN_POINT('',(1.1405019977285,4.,-15.1207265545853));
#17874=CARTESIAN_POINT('',(13.152726411984,4.,-16.3707841358972));
#17875=CARTESIAN_POINT('',(11.7931885652427,4.,0.926903443844235));
#17876=CARTESIAN_POINT('',(11.0109274142019,4.,-16.1831753591847));
#17877=CARTESIAN_POINT('',(-1.32291530947978,4.,-15.1028045363624));
#17878=CARTESIAN_POINT('',(10.8300692524884,4.,-18.325554953314));
#17879=CARTESIAN_POINT('',(12.2895168970939,4.,-1.03747227636268));
#17880=CARTESIAN_POINT('',(-3.73025667693335,4.,-14.60729197018));
#17881=CARTESIAN_POINT('',(-10.8300692524884,4.,-18.325554953314));
#17882=CARTESIAN_POINT('',(3.73025667693335,4.,-14.60729197018));
#17883=CARTESIAN_POINT('',(-11.0109274142019,4.,-16.1831753591847));
#17884=CARTESIAN_POINT('',(-12.2895168970939,4.,-1.03747227636268));
#17885=CARTESIAN_POINT('',(-13.152726411984,4.,-16.3707841358972));
#17886=CARTESIAN_POINT('',(1.32291530947978,4.,-15.1028045363624));
#17887=CARTESIAN_POINT('',(-12.9842634503587,4.,-14.227394243563));
#17888=CARTESIAN_POINT('',(-11.7931885652427,4.,0.926903443844235));
#17889=CARTESIAN_POINT('',(-15.1281735948574,4.,-14.0656868154229));
#17890=CARTESIAN_POINT('',(-1.1405019977285,4.,-15.1207265545853));
#17891=CARTESIAN_POINT('',(-14.6148366502913,4.,-11.9778685327787));
#17892=CARTESIAN_POINT('',(-11.0045483578897,4.,2.7057149931719));
#17893=CARTESIAN_POINT('',(-16.7042622998248,4.,-11.4711137053999));
#17894=CARTESIAN_POINT('',(-3.55556121796803,4.,-14.6601086086066));
#17895=CARTESIAN_POINT('',(-9.98182727519893,4.,4.26438303187517));
#17896=CARTESIAN_POINT('',(-4.28626379701574E-16,4.,-18.));
#17897=CARTESIAN_POINT('Origin',(0.,4.,-14.5));
#17898=CARTESIAN_POINT('Origin',(0.,-4.,0.));
#17899=CARTESIAN_POINT('',(-16.7042622998248,-4.,-11.4711137053999));
#17900=CARTESIAN_POINT('',(-9.98182727519893,-4.,4.26438303187517));
#17901=CARTESIAN_POINT('',(-14.6148366502913,-4.,-11.9778685327787));
#17902=CARTESIAN_POINT('',(-3.55556121796803,-4.,-14.6601086086066));
#17903=CARTESIAN_POINT('',(-15.1281735948574,-4.,-14.0656868154229));
#17904=CARTESIAN_POINT('',(-11.0045483578897,-4.,2.7057149931719));
#17905=CARTESIAN_POINT('',(-12.9842634503587,-4.,-14.227394243563));
#17906=CARTESIAN_POINT('',(-1.1405019977285,-4.,-15.1207265545853));
#17907=CARTESIAN_POINT('',(-13.152726411984,-4.,-16.3707841358972));
#17908=CARTESIAN_POINT('',(-11.7931885652427,-4.,0.926903443844235));
#17909=CARTESIAN_POINT('',(-11.0109274142019,-4.,-16.1831753591847));
#17910=CARTESIAN_POINT('',(1.32291530947978,-4.,-15.1028045363624));
#17911=CARTESIAN_POINT('',(-10.8300692524884,-4.,-18.325554953314));
#17912=CARTESIAN_POINT('',(-12.2895168970939,-4.,-1.03747227636268));
#17913=CARTESIAN_POINT('',(3.73025667693335,-4.,-14.60729197018));
#17914=CARTESIAN_POINT('',(10.8300692524884,-4.,-18.325554953314));
#17915=CARTESIAN_POINT('',(-3.73025667693335,-4.,-14.60729197018));
#17916=CARTESIAN_POINT('',(11.0109274142019,-4.,-16.1831753591847));
#17917=CARTESIAN_POINT('',(12.2895168970939,-4.,-1.03747227636268));
#17918=CARTESIAN_POINT('',(13.152726411984,-4.,-16.3707841358972));
#17919=CARTESIAN_POINT('',(-1.32291530947978,-4.,-15.1028045363624));
#17920=CARTESIAN_POINT('',(12.9842634503587,-4.,-14.227394243563));
#17921=CARTESIAN_POINT('',(11.7931885652427,-4.,0.926903443844235));
#17922=CARTESIAN_POINT('',(15.1281735948574,-4.,-14.0656868154229));
#17923=CARTESIAN_POINT('',(1.1405019977285,-4.,-15.1207265545853));
#17924=CARTESIAN_POINT('',(14.6148366502913,-4.,-11.9778685327787));
#17925=CARTESIAN_POINT('',(11.0045483578897,-4.,2.7057149931719));
#17926=CARTESIAN_POINT('',(16.7042622998248,-4.,-11.4711137053999));
#17927=CARTESIAN_POINT('',(3.55556121796803,-4.,-14.6601086086066));
#17928=CARTESIAN_POINT('',(9.98182727519893,-4.,4.26438303187517));
#17929=CARTESIAN_POINT('',(0.,-4.,-11.));
#17930=CARTESIAN_POINT('Origin',(0.,-4.,-14.5));
#17931=CARTESIAN_POINT('Origin',(0.,-4.,-14.5));
#17932=CARTESIAN_POINT('',(0.,-3.49999999999999,-11.5));
#17933=CARTESIAN_POINT('',(-3.67394039744206E-16,-3.49999999999999,-17.5));
#17934=CARTESIAN_POINT('Origin',(0.,-3.49999999999999,-14.5));
#17935=CARTESIAN_POINT('',(-3.67394039744206E-16,3.5,-17.5));
#17936=CARTESIAN_POINT('',(-3.67394039744206E-16,-4.,-17.5));
#17937=CARTESIAN_POINT('Origin',(0.,3.5,-14.5));
#17938=CARTESIAN_POINT('Origin',(0.,-3.49999999999999,-14.5));
#17939=CARTESIAN_POINT('Origin',(-9.98182727519893,4.,4.26438303187517));
#17940=CARTESIAN_POINT('',(-16.7042622998248,4.,-11.4711137053999));
#17941=CARTESIAN_POINT('Origin',(-3.55556121796803,4.,-14.6601086086066));
#17942=CARTESIAN_POINT('',(-14.6148366502913,4.,-11.9778685327787));
#17943=CARTESIAN_POINT('Origin',(-11.0045483578897,4.,2.7057149931719));
#17944=CARTESIAN_POINT('',(-15.1281735948574,4.,-14.0656868154229));
#17945=CARTESIAN_POINT('Origin',(-1.1405019977285,4.,-15.1207265545853));
#17946=CARTESIAN_POINT('',(-12.9842634503587,4.,-14.227394243563));
#17947=CARTESIAN_POINT('Origin',(-11.7931885652427,4.,0.926903443844235));
#17948=CARTESIAN_POINT('',(-13.152726411984,4.,-16.3707841358972));
#17949=CARTESIAN_POINT('Origin',(1.32291530947978,4.,-15.1028045363624));
#17950=CARTESIAN_POINT('',(-11.0109274142019,4.,-16.1831753591847));
#17951=CARTESIAN_POINT('Origin',(-12.2895168970939,4.,-1.03747227636268));
#17952=CARTESIAN_POINT('',(-10.8300692524884,4.,-18.325554953314));
#17953=CARTESIAN_POINT('Origin',(3.73025667693335,4.,-14.60729197018));
#17954=CARTESIAN_POINT('Origin',(9.98182727519893,4.,4.26438303187517));
#17955=CARTESIAN_POINT('',(16.7042622998248,4.,-11.4711137053999));
#17956=CARTESIAN_POINT('Origin',(3.55556121796803,4.,-14.6601086086066));
#17957=CARTESIAN_POINT('',(14.6148366502913,4.,-11.9778685327787));
#17958=CARTESIAN_POINT('Origin',(11.0045483578897,4.,2.7057149931719));
#17959=CARTESIAN_POINT('',(15.1281735948574,4.,-14.0656868154229));
#17960=CARTESIAN_POINT('Origin',(1.1405019977285,4.,-15.1207265545853));
#17961=CARTESIAN_POINT('',(12.9842634503587,4.,-14.227394243563));
#17962=CARTESIAN_POINT('Origin',(11.7931885652427,4.,0.926903443844235));
#17963=CARTESIAN_POINT('',(13.152726411984,4.,-16.3707841358972));
#17964=CARTESIAN_POINT('Origin',(-1.32291530947978,4.,-15.1028045363624));
#17965=CARTESIAN_POINT('',(11.0109274142019,4.,-16.1831753591847));
#17966=CARTESIAN_POINT('Origin',(12.2895168970939,4.,-1.03747227636268));
#17967=CARTESIAN_POINT('',(10.8300692524884,4.,-18.325554953314));
#17968=CARTESIAN_POINT('Origin',(-3.73025667693335,4.,-14.60729197018));
#17969=CARTESIAN_POINT('Origin',(0.,-4.,-14.5));
#17970=CARTESIAN_POINT('',(-4.28626379701574E-16,-4.,-11.));
#17971=CARTESIAN_POINT('Origin',(0.,3.5,-14.5));
#17972=CARTESIAN_POINT('',(-3.67394039744206E-16,3.5,-17.5));
#32957=UNCERTAINTY_MEASURE_WITH_UNIT(LENGTH_MEASURE(0.01),#33017,
'DISTANCE_ACCURACY_VALUE',
'Maximum model space distance between geometric entities at asserted c
onnectivities');
#32984=UNCERTAINTY_MEASURE_WITH_UNIT(LENGTH_MEASURE(0.01),#33017,
'DISTANCE_ACCURACY_VALUE',
'Maximum model space distance between geometric entities at asserted c
onnectivities');
#32989=(
GEOMETRIC_REPRESENTATION_CONTEXT(3)
GLOBAL_UNCERTAINTY_ASSIGNED_CONTEXT((#32957))
GLOBAL_UNIT_ASSIGNED_CONTEXT((#33017,#33019,#33020))
REPRESENTATION_CONTEXT('','3D')
);
#33016=(
GEOMETRIC_REPRESENTATION_CONTEXT(3)
GLOBAL_UNCERTAINTY_ASSIGNED_CONTEXT((#32984))
GLOBAL_UNIT_ASSIGNED_CONTEXT((#33017,#33019,#33020))
REPRESENTATION_CONTEXT('','3D')
);
#33017=(
LENGTH_UNIT()
NAMED_UNIT(*)
SI_UNIT(.MILLI.,.METRE.)
);
#33019=(
NAMED_UNIT(*)
PLANE_ANGLE_UNIT()
SI_UNIT($,.RADIAN.)
);
#33020=(
NAMED_UNIT(*)
SI_UNIT($,.STERADIAN.)
SOLID_ANGLE_UNIT()
);
#33025=SHAPE_DEFINITION_REPRESENTATION(#33056,#33128);
#33056=PRODUCT_DEFINITION_SHAPE('',$,#33160);
#33128=SHAPE_REPRESENTATION('',(#10580),#32989);
#33155=PRODUCT_DEFINITION_CONTEXT('part definition',#33250,'design');
#33160=PRODUCT_DEFINITION('P_Torque Wrench_Pawl_PRT-RH-1004-03_M_Rev00',
'PRT-RH-1004-03',#33191,#33155);
#33191=PRODUCT_DEFINITION_FORMATION('',$,#33256);
#33250=APPLICATION_CONTEXT(
'Core Data for Automotive Mechanical Design Process');
#33251=PRODUCT_CONTEXT('part definition',#33250,'mechanical');
#33256=PRODUCT('P_Torque Wrench_Pawl_PRT-RH-1004-03_M_Rev00',
'PRT-RH-1004-03',$,(#33251));
#33284=PRESENTATION_STYLE_ASSIGNMENT((#33291));
#33291=SURFACE_STYLE_USAGE(.BOTH.,#33298);
#33298=SURFACE_SIDE_STYLE('',(#33305));
#33305=SURFACE_STYLE_FILL_AREA(#33312);
#33312=FILL_AREA_STYLE('Opaque(186,91,6)',(#33319));
#33319=FILL_AREA_STYLE_COLOUR('Opaque(186,91,6)',#33326);
#33326=COLOUR_RGB('Opaque(186,91,6)', 0.09019608, 0.27058824, 0.51372549);
ENDSEC;
END-ISO-10303-21;
